ISO-10303-21;
HEADER;
/* Generated by software containing ST-Developer
 * from STEP Tools, Inc. (www.steptools.com) 
 */

FILE_DESCRIPTION(
/* description */ ('PAT-091'),
/* implementation_level */ '2;1');

FILE_NAME(
/* name */ 'M4x4 collar screw.step',
/* time_stamp */ '2026-10-27T15:34:44-07:00',
/* author */ (''),
/* organization */ (''),
/* preprocessor_version */ 'ST-DEVELOPER v20.2',
/* originating_system */ 'Autodesk Translation Framework v15.17.0.0',
/* authorisation */ '');

FILE_SCHEMA (('AUTOMOTIVE_DESIGN { 1 0 10303 214 3 1 1 }'));
ENDSEC;

DATA;
#10=MECHANICAL_DESIGN_GEOMETRIC_PRESENTATION_REPRESENTATION('',(#1026),#25100);
#736=CONICAL_SURFACE('',#15482,0.185,0.785398163397449);
#806=SHAPE_REPRESENTATION_RELATIONSHIP('SRR','None',#25571,#916);
#916=ADVANCED_BREP_SHAPE_REPRESENTATION('',(#1148),#25041);
#1026=STYLED_ITEM('',(#26198),#1148);
#1148=MANIFOLD_SOLID_BREP('Body1',#13305);
#1483=FACE_BOUND('',#3595,.T.);
#1886=PLANE('',#15471);
#1887=PLANE('',#15473);
#1888=PLANE('',#15474);
#1889=PLANE('',#15475);
#1890=PLANE('',#15476);
#1891=PLANE('',#15477);
#1892=PLANE('',#15478);
#1893=PLANE('',#15479);
#1894=PLANE('',#15480);
#2500=FACE_OUTER_BOUND('',#3586,.T.);
#2501=FACE_OUTER_BOUND('',#3587,.T.);
#2502=FACE_OUTER_BOUND('',#3588,.T.);
#2503=FACE_OUTER_BOUND('',#3589,.T.);
#2504=FACE_OUTER_BOUND('',#3590,.T.);
#2505=FACE_OUTER_BOUND('',#3591,.T.);
#2506=FACE_OUTER_BOUND('',#3592,.T.);
#2507=FACE_OUTER_BOUND('',#3593,.T.);
#2508=FACE_OUTER_BOUND('',#3594,.T.);
#2509=FACE_OUTER_BOUND('',#3596,.T.);
#2510=FACE_OUTER_BOUND('',#3597,.T.);
#3586=EDGE_LOOP('',(#10728));
#3587=EDGE_LOOP('',(#10729,#10730,#10731,#10732));
#3588=EDGE_LOOP('',(#10733,#10734,#10735,#10736));
#3589=EDGE_LOOP('',(#10737,#10738,#10739,#10740));
#3590=EDGE_LOOP('',(#10741,#10742,#10743,#10744));
#3591=EDGE_LOOP('',(#10745,#10746,#10747,#10748));
#3592=EDGE_LOOP('',(#10749,#10750,#10751,#10752));
#3593=EDGE_LOOP('',(#10753,#10754,#10755,#10756,#10757,#10758));
#3594=EDGE_LOOP('',(#10759));
#3595=EDGE_LOOP('',(#10760,#10761,#10762,#10763,#10764,#10765));
#3596=EDGE_LOOP('',(#10766,#10767,#10768,#10769));
#3597=EDGE_LOOP('',(#10770,#10771,#10772,#10773));
#4613=LINE('',#22994,#5353);
#4614=LINE('',#22996,#5354);
#4615=LINE('',#22998,#5355);
#4616=LINE('',#22999,#5356);
#4617=LINE('',#23002,#5357);
#4618=LINE('',#23004,#5358);
#4619=LINE('',#23005,#5359);
#4620=LINE('',#23008,#5360);
#4621=LINE('',#23010,#5361);
#4622=LINE('',#23011,#5362);
#4623=LINE('',#23014,#5363);
#4624=LINE('',#23016,#5364);
#4625=LINE('',#23017,#5365);
#4626=LINE('',#23020,#5366);
#4627=LINE('',#23022,#5367);
#4628=LINE('',#23023,#5368);
#4629=LINE('',#23025,#5369);
#4630=LINE('',#23026,#5370);
#4631=LINE('',#23034,#5371);
#4632=LINE('',#23036,#5372);
#5353=VECTOR('',#18735,1.);
#5354=VECTOR('',#18736,1.);
#5355=VECTOR('',#18737,1.);
#5356=VECTOR('',#18738,1.);
#5357=VECTOR('',#18741,1.);
#5358=VECTOR('',#18742,1.);
#5359=VECTOR('',#18743,1.);
#5360=VECTOR('',#18746,1.);
#5361=VECTOR('',#18747,1.);
#5362=VECTOR('',#18748,1.);
#5363=VECTOR('',#18751,1.);
#5364=VECTOR('',#18752,1.);
#5365=VECTOR('',#18753,1.);
#5366=VECTOR('',#18756,1.);
#5367=VECTOR('',#18757,1.);
#5368=VECTOR('',#18758,1.);
#5369=VECTOR('',#18761,1.);
#5370=VECTOR('',#18762,1.);
#5371=VECTOR('',#18773,0.185);
#5372=VECTOR('',#18776,0.2);
#5989=CIRCLE('',#15472,0.1954);
#5990=CIRCLE('',#15481,0.17);
#5991=CIRCLE('',#15483,0.1954);
#6966=VERTEX_POINT('',#22989);
#6967=VERTEX_POINT('',#22992);
#6968=VERTEX_POINT('',#22993);
#6969=VERTEX_POINT('',#22995);
#6970=VERTEX_POINT('',#22997);
#6971=VERTEX_POINT('',#23001);
#6972=VERTEX_POINT('',#23003);
#6973=VERTEX_POINT('',#23007);
#6974=VERTEX_POINT('',#23009);
#6975=VERTEX_POINT('',#23013);
#6976=VERTEX_POINT('',#23015);
#6977=VERTEX_POINT('',#23019);
#6978=VERTEX_POINT('',#23021);
#6979=VERTEX_POINT('',#23029);
#6980=VERTEX_POINT('',#23032);
#8299=EDGE_CURVE('',#6966,#6966,#5989,.T.);
#8300=EDGE_CURVE('',#6967,#6968,#4613,.T.);
#8301=EDGE_CURVE('',#6967,#6969,#4614,.T.);
#8302=EDGE_CURVE('',#6969,#6970,#4615,.T.);
#8303=EDGE_CURVE('',#6968,#6970,#4616,.T.);
#8304=EDGE_CURVE('',#6971,#6967,#4617,.T.);
#8305=EDGE_CURVE('',#6971,#6972,#4618,.T.);
#8306=EDGE_CURVE('',#6972,#6969,#4619,.T.);
#8307=EDGE_CURVE('',#6973,#6971,#4620,.T.);
#8308=EDGE_CURVE('',#6973,#6974,#4621,.T.);
#8309=EDGE_CURVE('',#6974,#6972,#4622,.T.);
#8310=EDGE_CURVE('',#6975,#6973,#4623,.T.);
#8311=EDGE_CURVE('',#6975,#6976,#4624,.T.);
#8312=EDGE_CURVE('',#6976,#6974,#4625,.T.);
#8313=EDGE_CURVE('',#6977,#6975,#4626,.T.);
#8314=EDGE_CURVE('',#6977,#6978,#4627,.T.);
#8315=EDGE_CURVE('',#6978,#6976,#4628,.T.);
#8316=EDGE_CURVE('',#6968,#6977,#4629,.T.);
#8317=EDGE_CURVE('',#6970,#6978,#4630,.T.);
#8318=EDGE_CURVE('',#6979,#6979,#5990,.T.);
#8319=EDGE_CURVE('',#6980,#6980,#5991,.T.);
#8320=EDGE_CURVE('',#6980,#6979,#4631,.T.);
#8321=EDGE_CURVE('',#6966,#6980,#4632,.T.);
#10728=ORIENTED_EDGE('',*,*,#8299,.F.);
#10729=ORIENTED_EDGE('',*,*,#8300,.F.);
#10730=ORIENTED_EDGE('',*,*,#8301,.T.);
#10731=ORIENTED_EDGE('',*,*,#8302,.T.);
#10732=ORIENTED_EDGE('',*,*,#8303,.F.);
#10733=ORIENTED_EDGE('',*,*,#8304,.F.);
#10734=ORIENTED_EDGE('',*,*,#8305,.T.);
#10735=ORIENTED_EDGE('',*,*,#8306,.T.);
#10736=ORIENTED_EDGE('',*,*,#8301,.F.);
#10737=ORIENTED_EDGE('',*,*,#8307,.F.);
#10738=ORIENTED_EDGE('',*,*,#8308,.T.);
#10739=ORIENTED_EDGE('',*,*,#8309,.T.);
#10740=ORIENTED_EDGE('',*,*,#8305,.F.);
#10741=ORIENTED_EDGE('',*,*,#8310,.F.);
#10742=ORIENTED_EDGE('',*,*,#8311,.T.);
#10743=ORIENTED_EDGE('',*,*,#8312,.T.);
#10744=ORIENTED_EDGE('',*,*,#8308,.F.);
#10745=ORIENTED_EDGE('',*,*,#8313,.F.);
#10746=ORIENTED_EDGE('',*,*,#8314,.T.);
#10747=ORIENTED_EDGE('',*,*,#8315,.T.);
#10748=ORIENTED_EDGE('',*,*,#8311,.F.);
#10749=ORIENTED_EDGE('',*,*,#8316,.F.);
#10750=ORIENTED_EDGE('',*,*,#8303,.T.);
#10751=ORIENTED_EDGE('',*,*,#8317,.T.);
#10752=ORIENTED_EDGE('',*,*,#8314,.F.);
#10753=ORIENTED_EDGE('',*,*,#8317,.F.);
#10754=ORIENTED_EDGE('',*,*,#8302,.F.);
#10755=ORIENTED_EDGE('',*,*,#8306,.F.);
#10756=ORIENTED_EDGE('',*,*,#8309,.F.);
#10757=ORIENTED_EDGE('',*,*,#8312,.F.);
#10758=ORIENTED_EDGE('',*,*,#8315,.F.);
#10759=ORIENTED_EDGE('',*,*,#8318,.F.);
#10760=ORIENTED_EDGE('',*,*,#8300,.T.);
#10761=ORIENTED_EDGE('',*,*,#8316,.T.);
#10762=ORIENTED_EDGE('',*,*,#8313,.T.);
#10763=ORIENTED_EDGE('',*,*,#8310,.T.);
#10764=ORIENTED_EDGE('',*,*,#8307,.T.);
#10765=ORIENTED_EDGE('',*,*,#8304,.T.);
#10766=ORIENTED_EDGE('',*,*,#8319,.F.);
#10767=ORIENTED_EDGE('',*,*,#8320,.T.);
#10768=ORIENTED_EDGE('',*,*,#8318,.T.);
#10769=ORIENTED_EDGE('',*,*,#8320,.F.);
#10770=ORIENTED_EDGE('',*,*,#8299,.T.);
#10771=ORIENTED_EDGE('',*,*,#8321,.T.);
#10772=ORIENTED_EDGE('',*,*,#8319,.T.);
#10773=ORIENTED_EDGE('',*,*,#8321,.F.);
#12258=CYLINDRICAL_SURFACE('',#15484,0.1954);
#12867=ADVANCED_FACE('',(#2500),#1886,.F.);
#12868=ADVANCED_FACE('',(#2501),#1887,.F.);
#12869=ADVANCED_FACE('',(#2502),#1888,.F.);
#12870=ADVANCED_FACE('',(#2503),#1889,.F.);
#12871=ADVANCED_FACE('',(#2504),#1890,.F.);
#12872=ADVANCED_FACE('',(#2505),#1891,.F.);
#12873=ADVANCED_FACE('',(#2506),#1892,.F.);
#12874=ADVANCED_FACE('',(#2507),#1893,.F.);
#12875=ADVANCED_FACE('',(#2508,#1483),#1894,.T.);
#12876=ADVANCED_FACE('',(#2509),#736,.T.);
#12877=ADVANCED_FACE('',(#2510),#12258,.T.);
#13305=CLOSED_SHELL('',(#12867,#12868,#12869,#12870,#12871,#12872,#12873,
#12874,#12875,#12876,#12877));
#15470=AXIS2_PLACEMENT_3D('',#22987,#18727,#18728);
#15471=AXIS2_PLACEMENT_3D('',#22988,#18729,#18730);
#15472=AXIS2_PLACEMENT_3D('',#22990,#18731,#18732);
#15473=AXIS2_PLACEMENT_3D('',#22991,#18733,#18734);
#15474=AXIS2_PLACEMENT_3D('',#23000,#18739,#18740);
#15475=AXIS2_PLACEMENT_3D('',#23006,#18744,#18745);
#15476=AXIS2_PLACEMENT_3D('',#23012,#18749,#18750);
#15477=AXIS2_PLACEMENT_3D('',#23018,#18754,#18755);
#15478=AXIS2_PLACEMENT_3D('',#23024,#18759,#18760);
#15479=AXIS2_PLACEMENT_3D('',#23027,#18763,#18764);
#15480=AXIS2_PLACEMENT_3D('',#23028,#18765,#18766);
#15481=AXIS2_PLACEMENT_3D('',#23030,#18767,#18768);
#15482=AXIS2_PLACEMENT_3D('',#23031,#18769,#18770);
#15483=AXIS2_PLACEMENT_3D('',#23033,#18771,#18772);
#15484=AXIS2_PLACEMENT_3D('',#23035,#18774,#18775);
#18727=DIRECTION('axis',(0.,0.,1.));
#18728=DIRECTION('refdir',(1.,0.,0.));
#18729=DIRECTION('center_axis',(0.,1.,0.));
#18730=DIRECTION('ref_axis',(1.,0.,0.));
#18731=DIRECTION('center_axis',(0.,1.,0.));
#18732=DIRECTION('ref_axis',(1.,0.,0.));
#18733=DIRECTION('center_axis',(0.866025403784439,0.,-0.5));
#18734=DIRECTION('ref_axis',(0.5,0.,0.866025403784439));
#18735=DIRECTION('',(0.5,0.,0.866025403784439));
#18736=DIRECTION('',(0.,-1.,0.));
#18737=DIRECTION('',(0.5,0.,0.866025403784439));
#18738=DIRECTION('',(0.,-1.,0.));
#18739=DIRECTION('center_axis',(1.20185167898973E-16,0.,-1.));
#18740=DIRECTION('ref_axis',(1.,0.,1.20185167898973E-16));
#18741=DIRECTION('',(1.,0.,1.20185167898973E-16));
#18742=DIRECTION('',(0.,-1.,0.));
#18743=DIRECTION('',(1.,0.,1.20185167898973E-16));
#18744=DIRECTION('center_axis',(-0.866025403784439,0.,-0.5));
#18745=DIRECTION('ref_axis',(0.5,0.,-0.866025403784439));
#18746=DIRECTION('',(0.5,0.,-0.866025403784439));
#18747=DIRECTION('',(0.,-1.,0.));
#18748=DIRECTION('',(0.5,0.,-0.866025403784439));
#18749=DIRECTION('center_axis',(-0.866025403784439,0.,0.5));
#18750=DIRECTION('ref_axis',(-0.5,0.,-0.866025403784439));
#18751=DIRECTION('',(-0.5,0.,-0.866025403784439));
#18752=DIRECTION('',(0.,-1.,0.));
#18753=DIRECTION('',(-0.5,0.,-0.866025403784439));
#18754=DIRECTION('center_axis',(-2.40370335797945E-16,0.,1.));
#18755=DIRECTION('ref_axis',(-1.,0.,-2.40370335797945E-16));
#18756=DIRECTION('',(-1.,0.,-2.40370335797945E-16));
#18757=DIRECTION('',(0.,-1.,0.));
#18758=DIRECTION('',(-1.,0.,-2.40370335797945E-16));
#18759=DIRECTION('center_axis',(0.866025403784439,0.,0.5));
#18760=DIRECTION('ref_axis',(-0.5,0.,0.866025403784439));
#18761=DIRECTION('',(-0.5,0.,0.866025403784439));
#18762=DIRECTION('',(-0.5,0.,0.866025403784439));
#18763=DIRECTION('center_axis',(0.,-1.,0.));
#18764=DIRECTION('ref_axis',(0.,0.,-1.));
#18765=DIRECTION('center_axis',(0.,1.,0.));
#18766=DIRECTION('ref_axis',(0.,0.,1.));
#18767=DIRECTION('center_axis',(0.,-1.,0.));
#18768=DIRECTION('ref_axis',(1.,0.,0.));
#18769=DIRECTION('center_axis',(0.,-1.,0.));
#18770=DIRECTION('ref_axis',(1.,0.,0.));
#18771=DIRECTION('center_axis',(0.,-1.,0.));
#18772=DIRECTION('ref_axis',(1.,0.,0.));
#18773=DIRECTION('',(0.707106781186548,0.707106781186547,8.65956056235494E-17));
#18774=DIRECTION('center_axis',(0.,-1.,0.));
#18775=DIRECTION('ref_axis',(1.,0.,0.));
#18776=DIRECTION('',(0.,1.,0.));
#22987=CARTESIAN_POINT('',(0.,0.,0.));
#22988=CARTESIAN_POINT('Origin',(0.,-0.4,0.));
#22989=CARTESIAN_POINT('',(-0.1954,-0.4,2.39295984553393E-17));
#22990=CARTESIAN_POINT('Origin',(0.,-0.4,0.));
#22991=CARTESIAN_POINT('Origin',(0.0577350269189626,0.,-0.1));
#22992=CARTESIAN_POINT('',(0.0577350269189626,0.,-0.1));
#22993=CARTESIAN_POINT('',(0.115470053837925,0.,0.));
#22994=CARTESIAN_POINT('',(0.0934187836487032,0.,-0.0381939203391614));
#22995=CARTESIAN_POINT('',(0.0577350269189626,-0.2,-0.1));
#22996=CARTESIAN_POINT('',(0.0577350269189626,0.,-0.1));
#22997=CARTESIAN_POINT('',(0.115470053837925,-0.2,0.));
#22998=CARTESIAN_POINT('',(0.115470053837925,-0.2,0.));
#22999=CARTESIAN_POINT('',(0.115470053837925,0.,0.));
#23000=CARTESIAN_POINT('Origin',(-0.0577350269189626,0.,-0.1));
#23001=CARTESIAN_POINT('',(-0.0577350269189626,0.,-0.1));
#23002=CARTESIAN_POINT('',(0.0561324865405187,0.,-0.1));
#23003=CARTESIAN_POINT('',(-0.0577350269189626,-0.2,-0.1));
#23004=CARTESIAN_POINT('',(-0.0577350269189626,0.,-0.1));
#23005=CARTESIAN_POINT('',(0.0577350269189626,-0.2,-0.1));
#23006=CARTESIAN_POINT('Origin',(-0.115470053837925,0.,-1.38777878078145E-17));
#23007=CARTESIAN_POINT('',(-0.115470053837925,0.,-1.41410031829988E-17));
#23008=CARTESIAN_POINT('',(-0.0797862971081845,0.,-0.0618060796608387));
#23009=CARTESIAN_POINT('',(-0.115470053837925,-0.2,-1.38777878078145E-17));
#23010=CARTESIAN_POINT('',(-0.115470053837925,0.,-1.41410031829988E-17));
#23011=CARTESIAN_POINT('',(-0.0577350269189626,-0.2,-0.1));
#23012=CARTESIAN_POINT('Origin',(-0.0577350269189626,0.,0.1));
#23013=CARTESIAN_POINT('',(-0.0577350269189626,0.,0.1));
#23014=CARTESIAN_POINT('',(-0.0509187836487033,0.,0.111806079660839));
#23015=CARTESIAN_POINT('',(-0.0577350269189626,-0.2,0.1));
#23016=CARTESIAN_POINT('',(-0.0577350269189626,0.,0.1));
#23017=CARTESIAN_POINT('',(-0.115470053837925,-0.2,-1.41410031829988E-17));
#23018=CARTESIAN_POINT('Origin',(0.0577350269189626,0.,0.1));
#23019=CARTESIAN_POINT('',(0.0577350269189626,0.,0.1));
#23020=CARTESIAN_POINT('',(0.113867513459481,0.,0.1));
#23021=CARTESIAN_POINT('',(0.0577350269189626,-0.2,0.1));
#23022=CARTESIAN_POINT('',(0.0577350269189626,0.,0.1));
#23023=CARTESIAN_POINT('',(-0.0577350269189626,-0.2,0.1));
#23024=CARTESIAN_POINT('Origin',(0.115470053837925,0.,0.));
#23025=CARTESIAN_POINT('',(0.122286297108185,0.,-0.0118060796608386));
#23026=CARTESIAN_POINT('',(0.0577350269189626,-0.2,0.1));
#23027=CARTESIAN_POINT('Origin',(0.,-0.2,0.));
#23028=CARTESIAN_POINT('Origin',(0.17,0.,0.));
#23029=CARTESIAN_POINT('',(-0.17,-8.67361737988404E-18,-2.0818995585505E-17));
#23030=CARTESIAN_POINT('Origin',(0.,0.,0.));
#23031=CARTESIAN_POINT('Origin',(0.,-0.015,0.));
#23032=CARTESIAN_POINT('',(-0.1954,-0.0254,-2.39295984553393E-17));
#23033=CARTESIAN_POINT('Origin',(0.,-0.0254,0.));
#23034=CARTESIAN_POINT('',(-0.185,-0.015,-2.2655965784226E-17));
#23035=CARTESIAN_POINT('Origin',(0.,-0.2775,0.));
#23036=CARTESIAN_POINT('',(-0.1954,-0.2775,-2.39295984553393E-17));
#24920=UNCERTAINTY_MEASURE_WITH_UNIT(LENGTH_MEASURE(0.001),#25101,
'DISTANCE_ACCURACY_VALUE',
'Maximum model space distance between geometric entities at asserted c
onnectivities');
#24979=UNCERTAINTY_MEASURE_WITH_UNIT(LENGTH_MEASURE(0.001),#25101,
'DISTANCE_ACCURACY_VALUE',
'Maximum model space distance between geometric entities at asserted c
onnectivities');
#25041=(
GEOMETRIC_REPRESENTATION_CONTEXT(3)
GLOBAL_UNCERTAINTY_ASSIGNED_CONTEXT((#24920))
GLOBAL_UNIT_ASSIGNED_CONTEXT((#25101,#25103,#25104))
REPRESENTATION_CONTEXT('','3D')
);
#25100=(
GEOMETRIC_REPRESENTATION_CONTEXT(3)
GLOBAL_UNCERTAINTY_ASSIGNED_CONTEXT((#24979))
GLOBAL_UNIT_ASSIGNED_CONTEXT((#25101,#25103,#25104))
REPRESENTATION_CONTEXT('','3D')
);
#25101=(
LENGTH_UNIT()
NAMED_UNIT(*)
SI_UNIT(.CENTI.,.METRE.)
);
#25103=(
NAMED_UNIT(*)
PLANE_ANGLE_UNIT()
SI_UNIT($,.RADIAN.)
);
#25104=(
NAMED_UNIT(*)
SI_UNIT($,.STERADIAN.)
SOLID_ANGLE_UNIT()
);
#25166=SHAPE_DEFINITION_REPRESENTATION(#25288,#25571);
#25288=PRODUCT_DEFINITION_SHAPE('',$,#25692);
#25571=SHAPE_REPRESENTATION('',(#15470),#25041);
#25630=PRODUCT_DEFINITION_CONTEXT('part definition',#25992,'design');
#25692=PRODUCT_DEFINITION('M4x4 collar screw','M4x4 collar screw',#25812,
#25630);
#25812=PRODUCT_DEFINITION_FORMATION('',$,#26055);
#25992=APPLICATION_CONTEXT(
'Core Data for Automotive Mechanical Design Process');
#25993=PRODUCT_CONTEXT('part definition',#25992,'mechanical');
#26055=PRODUCT('M4x4 collar screw','M4x4 collar screw',
'M4x4 collar screw',(#25993));
#26192=COLOUR_RGB('Black',0.12,0.14,0.17);
#26193=FILL_AREA_STYLE_COLOUR('',#26192);
#26194=FILL_AREA_STYLE('',(#26193));
#26195=SURFACE_STYLE_FILL_AREA(#26194);
#26196=SURFACE_SIDE_STYLE('',(#26195));
#26197=SURFACE_STYLE_USAGE(.BOTH.,#26196);
#26198=PRESENTATION_STYLE_ASSIGNMENT((#26197));
ENDSEC;
END-ISO-10303-21;
